ISO-10303-21;
HEADER;
FILE_DESCRIPTION (('STEP AP203'),
    '1' );
FILE_NAME ('1602p_c_13.step',
    '2026-10-31T14:11:27',
    ( '' ),
    ( '' ),
    'SwSTEP 2.0',
    'SolidWorks 2024',
    '' );
FILE_SCHEMA (( 'AUTOMOTIVE_DESIGN' ));
ENDSEC;

DATA;
#10=FACE_OUTER_BOUND ( 'NONE', #10461, .T. ) ;
#243=CIRCLE ( 'NONE', #9002, 2.499999999999999556 ) ;
#318=CIRCLE ( 'NONE', #13611, 3.499999999999999556 ) ;
#415=DIRECTION ( 'NONE',  ( 1.000000000000000000, 0.000000000000000000, 0.000000000000000000 ) ) ;
#724=DIRECTION ( 'NONE',  ( -0.9997648975362221080, -0.02168293463503390486, 0.000000000000000000 ) ) ;
#852=DIRECTION ( 'NONE',  ( 3.210834492194349687E-17, -2.441916418604790135E-15, -1.000000000000000000 ) ) ;
#931=ORIENTED_EDGE ( 'NONE', *, *, #4009, .T. ) ;
#1124=VECTOR ( 'NONE', #10110, 1000.000000000000000 ) ;
#1363=DESIGN_CONTEXT ( 'detailed design', #5520, 'design' ) ;
#1390=EDGE_LOOP ( 'NONE', ( #11350, #21925 ) ) ;
#1636=DIRECTION ( 'NONE',  ( -0.9997648975362222190, -0.02168293463503410262, 0.000000000000000000 ) ) ;
#1799=CYLINDRICAL_SURFACE ( 'NONE', #17458, 3.499999999999999556 ) ;
#1823=SHAPE_REPRESENTATION_RELATIONSHIP ( 'NONE' , 'NONE' ,  #9451, #22100 ) ;
#1976=EDGE_LOOP ( 'NONE', ( #8688, #16014, #13668, #9572 ) ) ;
#1982=CARTESIAN_POINT ( 'NONE',  ( -20.00000000397360012, 22.95208919256889857, -5.000000000000000000 ) ) ;
#2352=FACE_OUTER_BOUND ( 'NONE', #8437, .T. ) ;
#2388=CARTESIAN_POINT ( 'NONE',  ( -23.49917714535037661, 22.87619892134627975, -3.750000000000000000 ) ) ;
#2545=CARTESIAN_POINT ( 'NONE',  ( -17.50058776013304396, 23.00629652915649004, -2.500000000000039968 ) ) ;
#2569=CARTESIAN_POINT ( 'NONE',  ( 0.000000000000000000, 0.000000000000000000, 0.000000000000000000 ) ) ;
#2805=CARTESIAN_POINT ( 'NONE',  ( -17.50058776013304396, 23.00629652915649004, -5.000000000000000000 ) ) ;
#2918=AXIS2_PLACEMENT_3D ( 'NONE', #21630, #12747, #7171 ) ;
#3137=AXIS2_PLACEMENT_3D ( 'NONE', #9621, #12924, #14949 ) ;
#3205=ORIENTED_EDGE ( 'NONE', *, *, #12997, .F. ) ;
#3337=ORIENTED_EDGE ( 'NONE', *, *, #14417, .F. ) ;
#3343=CARTESIAN_POINT ( 'NONE',  ( -17.50058776013304396, 23.00629652915649004, -3.750000000000000000 ) ) ;
#3610=ORIENTED_EDGE ( 'NONE', *, *, #11121, .T. ) ;
#3813=VERTEX_POINT ( 'NONE', #16552 ) ;
#4009=EDGE_CURVE ( 'NONE', #14240, #9157, #17912, .T. ) ;
#4015=DIRECTION ( 'NONE',  ( 3.210834492194360164E-17, -2.441916418604790135E-15, -1.000000000000000000 ) ) ;
#4172=DIRECTION ( 'NONE',  ( 3.210834492194344756E-17, -2.441916418604790135E-15, -1.000000000000000000 ) ) ;
#4386=PRODUCT_DEFINITION_SHAPE ( 'NONE', 'NONE',  #5042 ) ;
#4449=DIRECTION ( 'NONE',  ( 3.210834492194360164E-17, -2.441916418604790135E-15, -1.000000000000000000 ) ) ;
#5042=PRODUCT_DEFINITION ( 'UNKNOWN', '', #6911, #1363 ) ;
#5145=EDGE_CURVE ( 'NONE', #6789, #9680, #15547, .T. ) ;
#5161=( NAMED_UNIT ( * ) PLANE_ANGLE_UNIT ( ) SI_UNIT ( $, .RADIAN. ) );
#5254=CARTESIAN_POINT ( 'NONE',  ( -22.49941224781415627, 22.89788185598131420, -5.000000000000000000 ) ) ;
#5374=DIRECTION ( 'NONE',  ( -0.9997648975362221080, -0.02168293463503390486, 0.000000000000000000 ) ) ;
#5520=APPLICATION_CONTEXT ( 'configuration controlled 3d designs of mechanical parts and assemblies' ) ;
#5805=LINE ( 'NONE', #3343, #15640 ) ;
#5985=CARTESIAN_POINT ( 'NONE',  ( -20.00000000397360012, 22.95208919256889857, -5.000000000000000000 ) ) ;
#6005=CARTESIAN_POINT ( 'NONE',  ( -20.00000000397360012, 22.95208919256889857, -2.500000000000039968 ) ) ;
#6219=PLANE ( 'NONE',  #21351 ) ;
#6534=CARTESIAN_POINT ( 'NONE',  ( -16.50082286259682363, 23.02797946379152094, -2.500000000000039968 ) ) ;
#6727=CIRCLE ( 'NONE', #23375, 2.499999999999999556 ) ;
#6789=VERTEX_POINT ( 'NONE', #6534 ) ;
#6896=MECHANICAL_CONTEXT ( 'NONE', #22004, 'mechanical' ) ;
#6911=PRODUCT_DEFINITION_FORMATION_WITH_SPECIFIED_SOURCE ( 'ANY', '', #8185, .NOT_KNOWN. ) ;
#7043=ADVANCED_FACE ( 'NONE', ( #2352 ), #20518, .F. ) ;
#7058=DIRECTION ( 'NONE',  ( -3.210834492194360164E-17, 2.441916418604790135E-15, 1.000000000000000000 ) ) ;
#7171=DIRECTION ( 'NONE',  ( -0.9997648975362221080, -0.02168293463503390486, 0.000000000000000000 ) ) ;
#7772=DIRECTION ( 'NONE',  ( -3.210834492194344756E-17, 2.441916418604790135E-15, 1.000000000000000000 ) ) ;
#7874=FACE_OUTER_BOUND ( 'NONE', #19186, .T. ) ;
#8026=PLANE ( 'NONE',  #18711 ) ;
#8123=DIRECTION ( 'NONE',  ( 1.013160721610911865E-47, -1.000000000000000000, 2.441916418604790135E-15 ) ) ;
#8171=CARTESIAN_POINT ( 'NONE',  ( -22.49941224781415627, 22.89788185598131420, -3.750000000000000000 ) ) ;
#8185=PRODUCT ( '1602p_c_13', '1602p_c_13', '', ( #6896 ) ) ;
#8437=EDGE_LOOP ( 'NONE', ( #16364, #16954, #9782, #3337 ) ) ;
#8509=ORIENTED_EDGE ( 'NONE', *, *, #19974, .F. ) ;
#8688=ORIENTED_EDGE ( 'NONE', *, *, #5145, .F. ) ;
#9002=AXIS2_PLACEMENT_3D ( 'NONE', #20569, #22463, #11579 ) ;
#9009=DIRECTION ( 'NONE',  ( -0.9997648975362222190, -0.02168293463503410262, 0.000000000000000000 ) ) ;
#9057=DIRECTION ( 'NONE',  ( -0.9997648975362222190, -0.02168293463503410262, 0.000000000000000000 ) ) ;
#9157=VERTEX_POINT ( 'NONE', #2545 ) ;
#9184=UNCERTAINTY_MEASURE_WITH_UNIT (LENGTH_MEASURE( 1.000000000000000082E-05 ), #23203, 'distance_accuracy_value', 'NONE');
#9329=MANIFOLD_SOLID_BREP ( 'Imported1', #15506 ) ;
#9349=CYLINDRICAL_SURFACE ( 'NONE', #22993, 3.499999999999999556 ) ;
#9391=ORIENTED_EDGE ( 'NONE', *, *, #17007, .F. ) ;
#9420=ADVANCED_FACE ( 'NONE', ( #10 ), #1799, .T. ) ;
#9451=SHAPE_REPRESENTATION ( '1602p_c_13', ( #12739 ), #16529 ) ;
#9503=CARTESIAN_POINT ( 'NONE',  ( -23.49917714535037661, 22.87619892134627975, -5.000000000000000000 ) ) ;
#9548=CYLINDRICAL_SURFACE ( 'NONE', #15278, 2.499999999999999556 ) ;
#9572=ORIENTED_EDGE ( 'NONE', *, *, #12396, .T. ) ;
#9584=AXIS2_PLACEMENT_3D ( 'NONE', #9809, #4449, #17027 ) ;
#9621=CARTESIAN_POINT ( 'NONE',  ( -20.00000000397360012, 22.95208919256889857, -3.750000000000000000 ) ) ;
#9680=VERTEX_POINT ( 'NONE', #9775 ) ;
#9775=CARTESIAN_POINT ( 'NONE',  ( -16.50082286259682363, 23.02797946379152094, -5.000000000000000000 ) ) ;
#9782=ORIENTED_EDGE ( 'NONE', *, *, #19974, .T. ) ;
#9809=CARTESIAN_POINT ( 'NONE',  ( -20.00000000397360012, 22.95208919256889857, -2.500000000000039968 ) ) ;
#9937=FACE_OUTER_BOUND ( 'NONE', #10028, .T. ) ;
#10028=EDGE_LOOP ( 'NONE', ( #3205, #9391 ) ) ;
#10110=DIRECTION ( 'NONE',  ( 3.210834492194344756E-17, -2.441916418604790135E-15, -1.000000000000000000 ) ) ;
#10205=LINE ( 'NONE', #8171, #22063 ) ;
#10461=EDGE_LOOP ( 'NONE', ( #18573, #12531, #13214, #14193 ) ) ;
#10578=DIRECTION ( 'NONE',  ( 3.210834492194344756E-17, -2.441916418604790135E-15, -1.000000000000000000 ) ) ;
#10624=CARTESIAN_POINT ( 'NONE',  ( -20.00000000397360012, 22.95208919256889857, -3.750000000000000000 ) ) ;
#10701=ORIENTED_EDGE ( 'NONE', *, *, #13299, .F. ) ;
#10808=DIRECTION ( 'NONE',  ( 3.210834492194344756E-17, -2.441916418604790135E-15, -1.000000000000000000 ) ) ;
#11121=EDGE_CURVE ( 'NONE', #9157, #14240, #243, .T. ) ;
#11350=ORIENTED_EDGE ( 'NONE', *, *, #14365, .T. ) ;
#11572=DIRECTION ( 'NONE',  ( -0.9997648975362222190, -0.02168293463503410262, 0.000000000000000000 ) ) ;
#11579=DIRECTION ( 'NONE',  ( -0.9997648975362221080, -0.02168293463503390486, 0.000000000000000000 ) ) ;
#11640=VERTEX_POINT ( 'NONE', #9503 ) ;
#11708=CIRCLE ( 'NONE', #15475, 3.499999999999999556 ) ;
#11724=CIRCLE ( 'NONE', #15491, 3.499999999999999556 ) ;
#11905=CIRCLE ( 'NONE', #17951, 3.499999999999999556 ) ;
#12316=EDGE_LOOP ( 'NONE', ( #20512, #10701 ) ) ;
#12396=EDGE_CURVE ( 'NONE', #11640, #9680, #11708, .T. ) ;
#12464=ORIENTED_EDGE ( 'NONE', *, *, #11121, .F. ) ;
#12531=ORIENTED_EDGE ( 'NONE', *, *, #5145, .T. ) ;
#12695=FACE_OUTER_BOUND ( 'NONE', #1976, .T. ) ;
#12739=AXIS2_PLACEMENT_3D ( 'NONE', #2569, #13380, #415 ) ;
#12747=DIRECTION ( 'NONE',  ( -3.210834492194360164E-17, 2.441916418604790135E-15, 1.000000000000000000 ) ) ;
#12924=DIRECTION ( 'NONE',  ( 3.210834492194360164E-17, -2.441916418604790135E-15, -1.000000000000000000 ) ) ;
#12997=EDGE_CURVE ( 'NONE', #3813, #6789, #11724, .T. ) ;
#13095=CARTESIAN_POINT ( 'NONE',  ( -20.00000000397360012, 22.95208919256889857, -2.500000000000039968 ) ) ;
#13214=ORIENTED_EDGE ( 'NONE', *, *, #13299, .T. ) ;
#13299=EDGE_CURVE ( 'NONE', #9680, #11640, #318, .T. ) ;
#13380=DIRECTION ( 'NONE',  ( 0.000000000000000000, 0.000000000000000000, 1.000000000000000000 ) ) ;
#13462=CARTESIAN_POINT ( 'NONE',  ( -20.00000000397360012, 22.95208919256889857, -5.000000000000000000 ) ) ;
#13488=DIRECTION ( 'NONE',  ( 3.210834492194349687E-17, -2.441916418604790135E-15, -1.000000000000000000 ) ) ;
#13611=AXIS2_PLACEMENT_3D ( 'NONE', #1982, #21684, #16238 ) ;
#13668=ORIENTED_EDGE ( 'NONE', *, *, #21382, .T. ) ;
#14193=ORIENTED_EDGE ( 'NONE', *, *, #21382, .F. ) ;
#14240=VERTEX_POINT ( 'NONE', #21295 ) ;
#14277=CARTESIAN_POINT ( 'NONE',  ( -20.00000000397360012, 22.95208919256889857, -5.000000000000000000 ) ) ;
#14365=EDGE_CURVE ( 'NONE', #14375, #22099, #6727, .T. ) ;
#14375=VERTEX_POINT ( 'NONE', #5254 ) ;
#14417=EDGE_CURVE ( 'NONE', #22099, #14375, #15821, .T. ) ;
#14949=DIRECTION ( 'NONE',  ( -0.9997648975362221080, -0.02168293463503390486, 0.000000000000000000 ) ) ;
#15278=AXIS2_PLACEMENT_3D ( 'NONE', #18459, #22118, #724 ) ;
#15475=AXIS2_PLACEMENT_3D ( 'NONE', #5985, #7772, #17021 ) ;
#15491=AXIS2_PLACEMENT_3D ( 'NONE', #13095, #4172, #11572 ) ;
#15506=CLOSED_SHELL ( 'NONE', ( #9420, #19309, #7043, #20403, #21568, #19371 ) ) ;
#15547=LINE ( 'NONE', #22783, #1124 ) ;
#15640=VECTOR ( 'NONE', #4015, 1000.000000000000000 ) ;
#15821=CIRCLE ( 'NONE', #2918, 2.499999999999999556 ) ;
#16014=ORIENTED_EDGE ( 'NONE', *, *, #17007, .T. ) ;
#16204=( NAMED_UNIT ( * ) SI_UNIT ( $, .STERADIAN. ) SOLID_ANGLE_UNIT ( ) );
#16238=DIRECTION ( 'NONE',  ( -0.9997648975362222190, -0.02168293463503410262, 0.000000000000000000 ) ) ;
#16364=ORIENTED_EDGE ( 'NONE', *, *, #19771, .F. ) ;
#16529=( GEOMETRIC_REPRESENTATION_CONTEXT ( 3 ) GLOBAL_UNCERTAINTY_ASSIGNED_CONTEXT ( ( #9184 ) ) GLOBAL_UNIT_ASSIGNED_CONTEXT ( ( #23203, #5161, #16204 ) ) REPRESENTATION_CONTEXT ( 'NONE', 'WORKASPACE' ) );
#16552=CARTESIAN_POINT ( 'NONE',  ( -23.49917714535037661, 22.87619892134627975, -2.500000000000039968 ) ) ;
#16619=DIRECTION ( 'NONE',  ( 3.210834492194344756E-17, -2.441916418604790135E-15, -1.000000000000000000 ) ) ;
#16954=ORIENTED_EDGE ( 'NONE', *, *, #4009, .F. ) ;
#17007=EDGE_CURVE ( 'NONE', #6789, #3813, #11905, .T. ) ;
#17021=DIRECTION ( 'NONE',  ( -0.9997648975362222190, -0.02168293463503410262, 0.000000000000000000 ) ) ;
#17027=DIRECTION ( 'NONE',  ( -0.9997648975362221080, -0.02168293463503390486, 0.000000000000000000 ) ) ;
#17130=FACE_BOUND ( 'NONE', #1390, .T. ) ;
#17165=DIRECTION ( 'NONE',  ( 1.013160721610911865E-47, -1.000000000000000000, 2.441916418604790135E-15 ) ) ;
#17458=AXIS2_PLACEMENT_3D ( 'NONE', #10624, #19875, #9057 ) ;
#17912=CIRCLE ( 'NONE', #9584, 2.499999999999999556 ) ;
#17951=AXIS2_PLACEMENT_3D ( 'NONE', #19471, #10578, #1636 ) ;
#18459=CARTESIAN_POINT ( 'NONE',  ( -20.00000000397360012, 22.95208919256889857, -3.750000000000000000 ) ) ;
#18573=ORIENTED_EDGE ( 'NONE', *, *, #12997, .T. ) ;
#18670=LINE ( 'NONE', #2388, #21470 ) ;
#18711=AXIS2_PLACEMENT_3D ( 'NONE', #6005, #13488, #17165 ) ;
#18949=FACE_BOUND ( 'NONE', #22572, .T. ) ;
#19186=EDGE_LOOP ( 'NONE', ( #12464, #19366, #22141, #8509 ) ) ;
#19309=ADVANCED_FACE ( 'NONE', ( #7874 ), #9548, .F. ) ;
#19366=ORIENTED_EDGE ( 'NONE', *, *, #19771, .T. ) ;
#19371=ADVANCED_FACE ( 'NONE', ( #17130, #22342 ), #6219, .T. ) ;
#19471=CARTESIAN_POINT ( 'NONE',  ( -20.00000000397360012, 22.95208919256889857, -2.500000000000039968 ) ) ;
#19771=EDGE_CURVE ( 'NONE', #9157, #22099, #5805, .T. ) ;
#19875=DIRECTION ( 'NONE',  ( 3.210834492194344756E-17, -2.441916418604790135E-15, -1.000000000000000000 ) ) ;
#19974=EDGE_CURVE ( 'NONE', #14240, #14375, #10205, .T. ) ;
#20037=CARTESIAN_POINT ( 'NONE',  ( -20.00000000397360012, 22.95208919256889857, -3.750000000000000000 ) ) ;
#20403=ADVANCED_FACE ( 'NONE', ( #18949, #9937 ), #8026, .F. ) ;
#20512=ORIENTED_EDGE ( 'NONE', *, *, #12396, .F. ) ;
#20518=CYLINDRICAL_SURFACE ( 'NONE', #3137, 2.499999999999999556 ) ;
#20569=CARTESIAN_POINT ( 'NONE',  ( -20.00000000397360012, 22.95208919256889857, -2.500000000000039968 ) ) ;
#20864=DIRECTION ( 'NONE',  ( 3.210834492194360164E-17, -2.441916418604790135E-15, -1.000000000000000000 ) ) ;
#20899=SHAPE_DEFINITION_REPRESENTATION ( #4386, #9451 ) ;
#21295=CARTESIAN_POINT ( 'NONE',  ( -22.49941224781415627, 22.89788185598131420, -2.500000000000039968 ) ) ;
#21351=AXIS2_PLACEMENT_3D ( 'NONE', #13462, #852, #8123 ) ;
#21382=EDGE_CURVE ( 'NONE', #3813, #11640, #18670, .T. ) ;
#21470=VECTOR ( 'NONE', #16619, 1000.000000000000000 ) ;
#21568=ADVANCED_FACE ( 'NONE', ( #12695 ), #9349, .T. ) ;
#21630=CARTESIAN_POINT ( 'NONE',  ( -20.00000000397360012, 22.95208919256889857, -5.000000000000000000 ) ) ;
#21684=DIRECTION ( 'NONE',  ( -3.210834492194344756E-17, 2.441916418604790135E-15, 1.000000000000000000 ) ) ;
#21925=ORIENTED_EDGE ( 'NONE', *, *, #14417, .T. ) ;
#22004=APPLICATION_CONTEXT ( 'configuration controlled 3d designs of mechanical parts and assemblies' ) ;
#22063=VECTOR ( 'NONE', #20864, 1000.000000000000000 ) ;
#22099=VERTEX_POINT ( 'NONE', #2805 ) ;
#22100=ADVANCED_BREP_SHAPE_REPRESENTATION ( '', ( #9329, #12739 ), #16529 ) ;
#22118=DIRECTION ( 'NONE',  ( 3.210834492194360164E-17, -2.441916418604790135E-15, -1.000000000000000000 ) ) ;
#22141=ORIENTED_EDGE ( 'NONE', *, *, #14365, .F. ) ;
#22342=FACE_OUTER_BOUND ( 'NONE', #12316, .T. ) ;
#22463=DIRECTION ( 'NONE',  ( 3.210834492194360164E-17, -2.441916418604790135E-15, -1.000000000000000000 ) ) ;
#22572=EDGE_LOOP ( 'NONE', ( #931, #3610 ) ) ;
#22783=CARTESIAN_POINT ( 'NONE',  ( -16.50082286259682363, 23.02797946379152094, -3.750000000000000000 ) ) ;
#22993=AXIS2_PLACEMENT_3D ( 'NONE', #20037, #10808, #9009 ) ;
#23203=( LENGTH_UNIT ( ) NAMED_UNIT ( * ) SI_UNIT ( .MILLI., .METRE. ) );
#23375=AXIS2_PLACEMENT_3D ( 'NONE', #14277, #7058, #5374 ) ;
#23536=COLOUR_RGB('Slate Gray', 0.40784314, 0.44705882, 0.49803922);
#23537=FILL_AREA_STYLE_COLOUR('',#23536);
#23538=FILL_AREA_STYLE('',(#23537));
#23539=SURFACE_STYLE_FILL_AREA(#23538);
#23540=SURFACE_SIDE_STYLE('',(#23539));
#23541=SURFACE_STYLE_USAGE(.BOTH.,#23540);
#23542=PRESENTATION_STYLE_ASSIGNMENT((#23541));
#23627=STYLED_ITEM('',(#23542),#9329);
#23628=MECHANICAL_DESIGN_GEOMETRIC_PRESENTATION_REPRESENTATION('',(#23627),#16529);
ENDSEC;
END-ISO-10303-21;
